ISO-10303-21;
HEADER;
/* Generated by software containing ST-Developer
 * from STEP Tools, Inc. (www.steptools.com) 
 */

FILE_DESCRIPTION(
/* description */ ('Rigid flange shaft coupling assembly'),
/* implementation_level */ '2;1');

FILE_NAME(
/* name */ 'End keeper (1).step',
/* time_stamp */ '2026-10-27T10:47:16-07:00',
/* author */ (''),
/* organization */ (''),
/* preprocessor_version */ 'ST-DEVELOPER v20.2',
/* originating_system */ 'Autodesk Translation Framework v15.17.0.0',
/* authorisation */ '');

FILE_SCHEMA (('AUTOMOTIVE_DESIGN { 1 0 10303 214 3 1 1 }'));
ENDSEC;

DATA;
#10=MECHANICAL_DESIGN_GEOMETRIC_PRESENTATION_REPRESENTATION('',(#417),#9141);
#360=SHAPE_REPRESENTATION_RELATIONSHIP('SRR','None',#9296,#388);
#388=ADVANCED_BREP_SHAPE_REPRESENTATION('',(#445),#9131);
#417=STYLED_ITEM('',(#9514),#445);
#445=MANIFOLD_SOLID_BREP('Body1',#4772);
#551=FACE_BOUND('',#1296,.T.);
#552=FACE_BOUND('',#1298,.T.);
#681=PLANE('',#5434);
#682=PLANE('',#5435);
#923=FACE_OUTER_BOUND('',#1293,.T.);
#924=FACE_OUTER_BOUND('',#1294,.T.);
#925=FACE_OUTER_BOUND('',#1295,.T.);
#926=FACE_OUTER_BOUND('',#1297,.T.);
#1293=EDGE_LOOP('',(#4023,#4024,#4025,#4026));
#1294=EDGE_LOOP('',(#4027,#4028,#4029,#4030));
#1295=EDGE_LOOP('',(#4031));
#1296=EDGE_LOOP('',(#4032));
#1297=EDGE_LOOP('',(#4033));
#1298=EDGE_LOOP('',(#4034));
#1632=LINE('',#8462,#1977);
#1633=LINE('',#8468,#1978);
#1977=VECTOR('',#6543,0.275);
#1978=VECTOR('',#6550,1.1);
#2226=CIRCLE('',#5429,0.275);
#2227=CIRCLE('',#5430,0.275);
#2228=CIRCLE('',#5432,1.1);
#2229=CIRCLE('',#5433,1.1);
#2543=VERTEX_POINT('',#8459);
#2544=VERTEX_POINT('',#8461);
#2545=VERTEX_POINT('',#8465);
#2546=VERTEX_POINT('',#8467);
#3055=EDGE_CURVE('',#2543,#2543,#2226,.T.);
#3056=EDGE_CURVE('',#2543,#2544,#1632,.T.);
#3057=EDGE_CURVE('',#2544,#2544,#2227,.T.);
#3058=EDGE_CURVE('',#2545,#2545,#2228,.T.);
#3059=EDGE_CURVE('',#2545,#2546,#1633,.T.);
#3060=EDGE_CURVE('',#2546,#2546,#2229,.T.);
#4023=ORIENTED_EDGE('',*,*,#3055,.F.);
#4024=ORIENTED_EDGE('',*,*,#3056,.T.);
#4025=ORIENTED_EDGE('',*,*,#3057,.T.);
#4026=ORIENTED_EDGE('',*,*,#3056,.F.);
#4027=ORIENTED_EDGE('',*,*,#3058,.F.);
#4028=ORIENTED_EDGE('',*,*,#3059,.T.);
#4029=ORIENTED_EDGE('',*,*,#3060,.T.);
#4030=ORIENTED_EDGE('',*,*,#3059,.F.);
#4031=ORIENTED_EDGE('',*,*,#3058,.T.);
#4032=ORIENTED_EDGE('',*,*,#3055,.T.);
#4033=ORIENTED_EDGE('',*,*,#3060,.F.);
#4034=ORIENTED_EDGE('',*,*,#3057,.F.);
#4462=CYLINDRICAL_SURFACE('',#5428,0.275);
#4463=CYLINDRICAL_SURFACE('',#5431,1.1);
#4659=ADVANCED_FACE('',(#923),#4462,.F.);
#4660=ADVANCED_FACE('',(#924),#4463,.T.);
#4661=ADVANCED_FACE('',(#925,#551),#681,.T.);
#4662=ADVANCED_FACE('',(#926,#552),#682,.F.);
#4772=CLOSED_SHELL('',(#4659,#4660,#4661,#4662));
#5427=AXIS2_PLACEMENT_3D('',#8457,#6537,#6538);
#5428=AXIS2_PLACEMENT_3D('',#8458,#6539,#6540);
#5429=AXIS2_PLACEMENT_3D('',#8460,#6541,#6542);
#5430=AXIS2_PLACEMENT_3D('',#8463,#6544,#6545);
#5431=AXIS2_PLACEMENT_3D('',#8464,#6546,#6547);
#5432=AXIS2_PLACEMENT_3D('',#8466,#6548,#6549);
#5433=AXIS2_PLACEMENT_3D('',#8469,#6551,#6552);
#5434=AXIS2_PLACEMENT_3D('',#8470,#6553,#6554);
#5435=AXIS2_PLACEMENT_3D('',#8471,#6555,#6556);
#6537=DIRECTION('axis',(0.,0.,1.));
#6538=DIRECTION('refdir',(1.,0.,0.));
#6539=DIRECTION('center_axis',(0.,1.,0.));
#6540=DIRECTION('ref_axis',(1.,0.,0.));
#6541=DIRECTION('center_axis',(0.,-1.,0.));
#6542=DIRECTION('ref_axis',(1.,0.,0.));
#6543=DIRECTION('',(0.,-1.,0.));
#6544=DIRECTION('center_axis',(0.,-1.,0.));
#6545=DIRECTION('ref_axis',(1.,0.,0.));
#6546=DIRECTION('center_axis',(0.,1.,0.));
#6547=DIRECTION('ref_axis',(1.,0.,0.));
#6548=DIRECTION('center_axis',(0.,1.,0.));
#6549=DIRECTION('ref_axis',(1.,0.,0.));
#6550=DIRECTION('',(0.,-1.,0.));
#6551=DIRECTION('center_axis',(0.,1.,0.));
#6552=DIRECTION('ref_axis',(1.,0.,0.));
#6553=DIRECTION('center_axis',(0.,1.,0.));
#6554=DIRECTION('ref_axis',(1.,0.,0.));
#6555=DIRECTION('center_axis',(0.,1.,0.));
#6556=DIRECTION('ref_axis',(1.,0.,0.));
#8457=CARTESIAN_POINT('',(0.,0.,0.));
#8458=CARTESIAN_POINT('Origin',(0.,24.5,6.53));
#8459=CARTESIAN_POINT('',(-0.275,24.7,6.53));
#8460=CARTESIAN_POINT('Origin',(0.,24.7,6.53));
#8461=CARTESIAN_POINT('',(-0.275,24.5,6.53));
#8462=CARTESIAN_POINT('',(-0.275,24.5,6.53));
#8463=CARTESIAN_POINT('Origin',(0.,24.5,6.53));
#8464=CARTESIAN_POINT('Origin',(0.,24.5,6.53));
#8465=CARTESIAN_POINT('',(-1.1,24.7,6.53));
#8466=CARTESIAN_POINT('Origin',(0.,24.7,6.53));
#8467=CARTESIAN_POINT('',(-1.1,24.5,6.53));
#8468=CARTESIAN_POINT('',(-1.1,24.5,6.53));
#8469=CARTESIAN_POINT('Origin',(0.,24.5,6.53));
#8470=CARTESIAN_POINT('Origin',(0.,24.7,6.53));
#8471=CARTESIAN_POINT('Origin',(0.,24.5,6.53));
#9098=UNCERTAINTY_MEASURE_WITH_UNIT(LENGTH_MEASURE(0.001),#9142,
'DISTANCE_ACCURACY_VALUE',
'Maximum model space distance between geometric entities at asserted c
onnectivities');
#9108=UNCERTAINTY_MEASURE_WITH_UNIT(LENGTH_MEASURE(0.001),#9142,
'DISTANCE_ACCURACY_VALUE',
'Maximum model space distance between geometric entities at asserted c
onnectivities');
#9131=(
GEOMETRIC_REPRESENTATION_CONTEXT(3)
GLOBAL_UNCERTAINTY_ASSIGNED_CONTEXT((#9098))
GLOBAL_UNIT_ASSIGNED_CONTEXT((#9142,#9144,#9145))
REPRESENTATION_CONTEXT('','3D')
);
#9141=(
GEOMETRIC_REPRESENTATION_CONTEXT(3)
GLOBAL_UNCERTAINTY_ASSIGNED_CONTEXT((#9108))
GLOBAL_UNIT_ASSIGNED_CONTEXT((#9142,#9144,#9145))
REPRESENTATION_CONTEXT('','3D')
);
#9142=(
LENGTH_UNIT()
NAMED_UNIT(*)
SI_UNIT(.CENTI.,.METRE.)
);
#9144=(
NAMED_UNIT(*)
PLANE_ANGLE_UNIT()
SI_UNIT($,.RADIAN.)
);
#9145=(
NAMED_UNIT(*)
SI_UNIT($,.STERADIAN.)
SOLID_ANGLE_UNIT()
);
#9168=SHAPE_DEFINITION_REPRESENTATION(#9202,#9296);
#9202=PRODUCT_DEFINITION_SHAPE('',$,#9329);
#9296=SHAPE_REPRESENTATION('',(#5427),#9131);
#9306=PRODUCT_DEFINITION_CONTEXT('part definition',#9404,'design');
#9329=PRODUCT_DEFINITION('End keeper (1)','End keeper (1)',#9361,#9306);
#9361=PRODUCT_DEFINITION_FORMATION('',$,#9428);
#9404=APPLICATION_CONTEXT(
'Core Data for Automotive Mechanical Design Process');
#9405=PRODUCT_CONTEXT('part definition',#9404,'mechanical');
#9428=PRODUCT('End keeper (1)','End keeper (1)','End keeper (1)',(#9405));
#9508=COLOUR_RGB('Off White',0.89,0.88,0.83);
#9509=FILL_AREA_STYLE_COLOUR('',#9508);
#9510=FILL_AREA_STYLE('',(#9509));
#9511=SURFACE_STYLE_FILL_AREA(#9510);
#9512=SURFACE_SIDE_STYLE('',(#9511));
#9513=SURFACE_STYLE_USAGE(.BOTH.,#9512);
#9514=PRESENTATION_STYLE_ASSIGNMENT((#9513));
ENDSEC;
END-ISO-10303-21;
